ISO-10303-21;
HEADER;
FILE_DESCRIPTION (('STEP AP214'),
    '1' );
FILE_NAME ('Screw 6.step',
    '2026-10-26T17:37:43',
    ( '' ),
    ( '' ),
    'SwSTEP 2.0',
    'SolidWorks 2024',
    '' );
FILE_SCHEMA (( 'AUTOMOTIVE_DESIGN' ));
ENDSEC;

DATA;
#81=EDGE_CURVE ( 'NONE', #2498, #2000, #21462, .T. ) ;
#95=DIRECTION ( 'NONE',  ( -2.336881798971000105E-14, 0.000000000000000000, -1.000000000000000000 ) ) ;
#170=ORIENTED_EDGE ( 'NONE', *, *, #1350, .F. ) ;
#197=DIRECTION ( 'NONE',  ( 0.000000000000000000, 0.000000000000000000, -1.000000000000000000 ) ) ;
#204=VERTEX_POINT ( 'NONE', #22501 ) ;
#217=AXIS2_PLACEMENT_3D ( 'NONE', #2919, #10176, #1149 ) ;
#252=ORIENTED_EDGE ( 'NONE', *, *, #13501, .F. ) ;
#257=VERTEX_POINT ( 'NONE', #7279 ) ;
#265=DIRECTION ( 'NONE',  ( 1.000000000000000000, 0.000000000000000000, 0.000000000000000000 ) ) ;
#354=CARTESIAN_POINT ( 'NONE',  ( 10.36831320289401859, -3640.848700000111421, 2296.210799999999836 ) ) ;
#390=CARTESIAN_POINT ( 'NONE',  ( 12.69999999994000106, -3636.810100000000148, 2296.210799999999836 ) ) ;
#422=ADVANCED_FACE ( 'NONE', ( #15004 ), #20281, .T. ) ;
#426=DIRECTION ( 'NONE',  ( 0.000000000000000000, 0.000000000000000000, 1.000000000000000000 ) ) ;
#582=DIRECTION ( 'NONE',  ( 0.8660254037825247941, -0.5000000000033149039, -5.278136500991149341E-12 ) ) ;
#657=CARTESIAN_POINT ( 'NONE',  ( 10.36831320284000135, -3638.156300000000101, 2292.781800000000203 ) ) ;
#671=VERTEX_POINT ( 'NONE', #9668 ) ;
#710=LINE ( 'NONE', #15013, #21202 ) ;
#768=LINE ( 'NONE', #7930, #7396 ) ;
#778=ORIENTED_EDGE ( 'NONE', *, *, #12253, .T. ) ;
#808=ORIENTED_EDGE ( 'NONE', *, *, #6925, .T. ) ;
#867=CLOSED_SHELL ( 'NONE', ( #14940, #12863, #19811, #19888, #18956, #9075, #9658, #16602, #7572, #8719, #20455, #11654, #2285, #18371, #8932, #20976, #21272, #17443, #7122, #8280, #17572, #9311, #22381, #422, #10868, #20015 ) ) ;
#910=EDGE_CURVE ( 'NONE', #22386, #17848, #19970, .T. ) ;
#1027=CARTESIAN_POINT ( 'NONE',  ( 10.36831320284000135, -3638.156300000000101, 2292.781800000000203 ) ) ;
#1028=VECTOR ( 'NONE', #2848, 1000.000000000000000 ) ;
#1038=LINE ( 'NONE', #10178, #18902 ) ;
#1085=CARTESIAN_POINT ( 'NONE',  ( 9.987313202835000681, -3637.936329547000241, 2296.591799999999694 ) ) ;
#1113=ORIENTED_EDGE ( 'NONE', *, *, #6592, .T. ) ;
#1133=ORIENTED_EDGE ( 'NONE', *, *, #2952, .T. ) ;
#1149=DIRECTION ( 'NONE',  ( 1.000000000000000000, 0.000000000000000000, 0.000000000000000000 ) ) ;
#1163=DIRECTION ( 'NONE',  ( 0.8660254037840939834, -0.5000000000005969669, 0.000000000000000000 ) ) ;
#1186=CARTESIAN_POINT ( 'NONE',  ( 12.69999999999999929, -3634.041499999999814, 2296.210799999999836 ) ) ;
#1226=ORIENTED_EDGE ( 'NONE', *, *, #19841, .T. ) ;
#1231=ADVANCED_BREP_SHAPE_REPRESENTATION ( '', ( #21284, #5611 ), #12740 ) ;
#1283=CYLINDRICAL_SURFACE ( 'NONE', #8511, 0.3809999999999154618 ) ;
#1293=CARTESIAN_POINT ( 'NONE',  ( 12.69999999999999929, -3639.502500000000055, 2290.622800000000097 ) ) ;
#1315=TOROIDAL_SURFACE ( 'NONE', #18169, 5.080000000000000071, 0.3810000000000000053 ) ;
#1331=CARTESIAN_POINT ( 'NONE',  ( 12.69999999999999929, -3639.502500000000055, 2290.622800000000097 ) ) ;
#1350=EDGE_CURVE ( 'NONE', #6875, #3774, #2663, .T. ) ;
#1394=AXIS2_PLACEMENT_3D ( 'NONE', #18019, #7028, #12289 ) ;
#1424=EDGE_LOOP ( 'NONE', ( #18539, #22099, #12919, #9036 ) ) ;
#1440=CARTESIAN_POINT ( 'NONE',  ( 15.41268679713999923, -3641.068670452857532, 2296.591799999999694 ) ) ;
#1499=DIRECTION ( 'NONE',  ( 0.000000000000000000, 0.000000000000000000, 1.000000000000000000 ) ) ;
#1511=EDGE_LOOP ( 'NONE', ( #17122, #8906 ) ) ;
#1512=PRODUCT_DEFINITION_SHAPE ( 'NONE', 'NONE',  #5365 ) ;
#1599=CARTESIAN_POINT ( 'NONE',  ( 10.36831320289401859, -3640.848700000111421, 2296.210799999999836 ) ) ;
#1639=DIRECTION ( 'NONE',  ( -0.5000000000031612490, -0.8660254037826135010, 0.000000000000000000 ) ) ;
#1667=CARTESIAN_POINT ( 'NONE',  ( 10.36831320284000135, -3635.463900000000194, 2292.781800000000203 ) ) ;
#1737=AXIS2_PLACEMENT_3D ( 'NONE', #20723, #11694, #4669 ) ;
#1769=ORIENTED_EDGE ( 'NONE', *, *, #7092, .T. ) ;
#1834=CYLINDRICAL_SURFACE ( 'NONE', #2773, 3.175000000000149925 ) ;
#1890=LINE ( 'NONE', #5651, #17316 ) ;
#1924=VECTOR ( 'NONE', #3908, 1000.000000000000114 ) ;
#2000=VERTEX_POINT ( 'NONE', #11562 ) ;
#2024=VERTEX_POINT ( 'NONE', #9363 ) ;
#2033=DIRECTION ( 'NONE',  ( 0.8660254037841628172, -0.5000000000004778400, 0.000000000000000000 ) ) ;
#2048=ORIENTED_EDGE ( 'NONE', *, *, #20807, .T. ) ;
#2065=EDGE_CURVE ( 'NONE', #2024, #2236, #13801, .T. ) ;
#2066=ORIENTED_EDGE ( 'NONE', *, *, #19760, .T. ) ;
#2069=VECTOR ( 'NONE', #2033, 999.9999999999998863 ) ;
#2076=CIRCLE ( 'NONE', #5831, 1.269999999999882334 ) ;
#2091=DIRECTION ( 'NONE',  ( 2.336881798971000105E-14, 0.000000000000000000, 1.000000000000000000 ) ) ;
#2161=VERTEX_POINT ( 'NONE', #6544 ) ;
#2189=( BOUNDED_CURVE ( )  B_SPLINE_CURVE ( 3, ( #18273, #18158, #13117, #354 ),
 .UNSPECIFIED., .F., .T. ) 
 B_SPLINE_CURVE_WITH_KNOTS ( ( 4, 4 ),
 ( 1.570796327105885126, 3.141592653589766471 ),
 .UNSPECIFIED. ) 
 CURVE ( )  GEOMETRIC_REPRESENTATION_ITEM ( )  RATIONAL_B_SPLINE_CURVE ( ( 1.000000000000000000, 0.8047378541976719646, 0.8047378541976719646, 1.000000000000000000 ) ) 
 REPRESENTATION_ITEM ( '' )  );
#2214=CARTESIAN_POINT ( 'NONE',  ( 14.05634339857000015, -3641.851755678999780, 2296.210799999999836 ) ) ;
#2236=VERTEX_POINT ( 'NONE', #1599 ) ;
#2257=( GEOMETRIC_REPRESENTATION_CONTEXT ( 3 ) GLOBAL_UNCERTAINTY_ASSIGNED_CONTEXT ( ( #16741 ) ) GLOBAL_UNIT_ASSIGNED_CONTEXT ( ( #21126, #3419, #23094 ) ) REPRESENTATION_CONTEXT ( 'NONE', 'WORKASPACE' ) );
#2285=ADVANCED_FACE ( 'NONE', ( #12275 ), #11204, .T. ) ;
#2371=ORIENTED_EDGE ( 'NONE', *, *, #2952, .F. ) ;
#2387=CARTESIAN_POINT ( 'NONE',  ( 12.69999999999999929, -3641.407499999999800, 2264.841800000000148 ) ) ;
#2427=VERTEX_POINT ( 'NONE', #1186 ) ;
#2441=DIRECTION ( 'NONE',  ( -0.8660254037820785955, -0.5000000000040877302, 3.192239903039919200E-14 ) ) ;
#2443=DIRECTION ( 'NONE',  ( 1.000000000000000000, 0.000000000000000000, -2.336881798971000105E-14 ) ) ;
#2448=UNCERTAINTY_MEASURE_WITH_UNIT (LENGTH_MEASURE( 1.000000000000000082E-05 ), #7409, 'distance_accuracy_value', 'NONE');
#2466=VECTOR ( 'NONE', #17296, 1000.000000000000000 ) ;
#2469=AXIS2_PLACEMENT_3D ( 'NONE', #7797, #6388, #8025 ) ;
#2498=VERTEX_POINT ( 'NONE', #3067 ) ;
#2518=DIRECTION ( 'NONE',  ( -0.8660254037840939834, 0.5000000000005969669, 0.000000000000000000 ) ) ;
#2558=ORIENTED_EDGE ( 'NONE', *, *, #9764, .F. ) ;
#2595=LINE ( 'NONE', #4363, #22271 ) ;
#2606=CARTESIAN_POINT ( 'NONE',  ( 0.000000000000000000, 0.000000000000000000, 0.000000000000000000 ) ) ;
#2621=EDGE_LOOP ( 'NONE', ( #9341, #4566, #18911, #14969 ) ) ;
#2653=ORIENTED_EDGE ( 'NONE', *, *, #4783, .F. ) ;
#2663=CIRCLE ( 'NONE', #17637, 1.904999999999823501 ) ;
#2664=EDGE_CURVE ( 'NONE', #22154, #19668, #13968, .T. ) ;
#2670=CARTESIAN_POINT ( 'NONE',  ( 12.69999999999999929, -3639.502500000000055, 2290.241799999999785 ) ) ;
#2691=EDGE_CURVE ( 'NONE', #11827, #2024, #1890, .T. ) ;
#2730=LINE ( 'NONE', #15396, #15971 ) ;
#2741=LINE ( 'NONE', #9670, #17048 ) ;
#2772=DIRECTION ( 'NONE',  ( 2.336881798971000105E-14, 2.336881798971000105E-14, 1.000000000000000000 ) ) ;
#2773=AXIS2_PLACEMENT_3D ( 'NONE', #12728, #426, #7565 ) ;
#2820=ORIENTED_EDGE ( 'NONE', *, *, #9789, .F. ) ;
#2839=AXIS2_PLACEMENT_3D ( 'NONE', #7371, #21886, #19907 ) ;
#2847=ORIENTED_EDGE ( 'NONE', *, *, #8379, .T. ) ;
#2848=DIRECTION ( 'NONE',  ( 0.000000000000000000, 0.000000000000000000, 1.000000000000000000 ) ) ;
#2858=VERTEX_POINT ( 'NONE', #18635 ) ;
#2860=AXIS2_PLACEMENT_3D ( 'NONE', #7544, #5683, #9192 ) ;
#2884=ORIENTED_EDGE ( 'NONE', *, *, #10419, .T. ) ;
#2919=CARTESIAN_POINT ( 'NONE',  ( 12.69999999999999929, -3639.502500000000055, 2290.241799999999785 ) ) ;
#2952=EDGE_CURVE ( 'NONE', #2498, #12177, #710, .T. ) ;
#3041=DIRECTION ( 'NONE',  ( 0.000000000000000000, 0.000000000000000000, -1.000000000000000000 ) ) ;
#3067=CARTESIAN_POINT ( 'NONE',  ( 12.69999999999999929, -3636.327499999999873, 2264.841800000000148 ) ) ;
#3139=DIRECTION ( 'NONE',  ( -5.682243826821398966E-14, -1.000000000000000000, 0.000000000000000000 ) ) ;
#3157=DIRECTION ( 'NONE',  ( 0.5000000000007065459, 0.8660254037840305896, 0.000000000000000000 ) ) ;
#3216=CARTESIAN_POINT ( 'NONE',  ( 18.16100000000000136, -3639.502500000000055, 2296.210799999999836 ) ) ;
#3242=CARTESIAN_POINT ( 'NONE',  ( 12.69999999997255280, -3636.370159094721657, 2296.591799999999694 ) ) ;
#3280=CARTESIAN_POINT ( 'NONE',  ( 14.05634339854999837, -3637.153244320999875, 2296.210799999999836 ) ) ;
#3303=PLANE ( 'NONE',  #14254 ) ;
#3332=VERTEX_POINT ( 'NONE', #13791 ) ;
#3342=EDGE_CURVE ( 'NONE', #16219, #14242, #13720, .T. ) ;
#3365=DIRECTION ( 'NONE',  ( -1.000000000000000000, 5.461016542361937364E-28, 2.336881798970999789E-14 ) ) ;
#3401=CARTESIAN_POINT ( 'NONE',  ( 11.34365660141000021, -3641.851755678999780, 2296.210799999999836 ) ) ;
#3419=( NAMED_UNIT ( * ) PLANE_ANGLE_UNIT ( ) SI_UNIT ( $, .RADIAN. ) );
#3432=CARTESIAN_POINT ( 'NONE',  ( 15.03168679707239441, -3640.848700000039116, 2296.210799999999836 ) ) ;
#3466=ORIENTED_EDGE ( 'NONE', *, *, #6267, .F. ) ;
#3468=CARTESIAN_POINT ( 'NONE',  ( 12.69999999997359019, -3636.810099999929662, 2296.210799999999836 ) ) ;
#3523=CARTESIAN_POINT ( 'NONE',  ( 12.69999999999999929, -3639.502500000000055, 2263.571799999999712 ) ) ;
#3537=ORIENTED_EDGE ( 'NONE', *, *, #6592, .F. ) ;
#3560=ORIENTED_EDGE ( 'NONE', *, *, #12253, .F. ) ;
#3575=ORIENTED_EDGE ( 'NONE', *, *, #4783, .T. ) ;
#3587=FACE_OUTER_BOUND ( 'NONE', #8459, .T. ) ;
#3610=FACE_OUTER_BOUND ( 'NONE', #16005, .T. ) ;
#3643=EDGE_CURVE ( 'NONE', #2024, #13470, #22490, .T. ) ;
#3712=CARTESIAN_POINT ( 'NONE',  ( 12.69999999999999929, -3634.041499999999814, 2290.622800000000097 ) ) ;
#3717=EDGE_CURVE ( 'NONE', #13767, #7858, #8705, .T. ) ;
#3727=ORIENTED_EDGE ( 'NONE', *, *, #12607, .T. ) ;
#3757=DIRECTION ( 'NONE',  ( 9.814416866149999939E-14, 3.885294924330999618E-13, 1.000000000000000000 ) ) ;
#3774=VERTEX_POINT ( 'NONE', #7522 ) ;
#3823=AXIS2_PLACEMENT_3D ( 'NONE', #16376, #12857, #3831 ) ;
#3831=DIRECTION ( 'NONE',  ( 0.000000000000000000, 0.000000000000000000, 1.000000000000000000 ) ) ;
#3852=AXIS2_PLACEMENT_3D ( 'NONE', #3401, #14423, #1639 ) ;
#3886=CARTESIAN_POINT ( 'NONE',  ( 12.69999999999999929, -3637.597499999999854, 2264.841800000000148 ) ) ;
#3906=EDGE_LOOP ( 'NONE', ( #2371, #12479, #8784, #20494 ) ) ;
#3908=DIRECTION ( 'NONE',  ( -0.8660254037817868289, -0.5000000000045929927, 1.319534125262979913E-12 ) ) ;
#3989=CIRCLE ( 'NONE', #2860, 0.3809999999999647002 ) ;
#3995=VECTOR ( 'NONE', #582, 1000.000000000000000 ) ;
#4050=VERTEX_POINT ( 'NONE', #8214 ) ;
#4082=ORIENTED_EDGE ( 'NONE', *, *, #13147, .T. ) ;
#4112=EDGE_LOOP ( 'NONE', ( #13945, #21532, #14018, #4082, #2884 ) ) ;
#4166=DIRECTION ( 'NONE',  ( -0.8660254037842740615, 0.5000000000002851053, 3.628718844334890455E-12 ) ) ;
#4181=CARTESIAN_POINT ( 'NONE',  ( 12.69999999999999929, -3639.502500000000055, 2296.210799999999836 ) ) ;
#4236=( BOUNDED_CURVE ( )  B_SPLINE_CURVE ( 3, ( #3432, #10347, #17494, #1440 ),
 .UNSPECIFIED., .F., .T. ) 
 B_SPLINE_CURVE_WITH_KNOTS ( ( 4, 4 ),
 ( -9.769962616701377556E-15, 1.570796326960964162 ),
 .UNSPECIFIED. ) 
 CURVE ( )  GEOMETRIC_REPRESENTATION_ITEM ( )  RATIONAL_B_SPLINE_CURVE ( ( 1.000000000000000000, 0.8047378540852202500, 0.8047378540852202500, 1.000000000000000000 ) ) 
 REPRESENTATION_ITEM ( '' )  );
#4333=CARTESIAN_POINT ( 'NONE',  ( 7.619999999999999218, -3639.502500000000055, 2290.241799999999785 ) ) ;
#4363=CARTESIAN_POINT ( 'NONE',  ( 15.03168679714000078, -3638.156300000000101, 2292.781800000000203 ) ) ;
#4391=CIRCLE ( 'NONE', #5915, 5.460999999999938126 ) ;
#4393=PLANE ( 'NONE',  #2469 ) ;
#4427=FACE_BOUND ( 'NONE', #1511, .T. ) ;
#4446=DIRECTION ( 'NONE',  ( 0.000000000000000000, -1.000000000000000000, 0.000000000000000000 ) ) ;
#4485=LINE ( 'NONE', #5922, #22877 ) ;
#4566=ORIENTED_EDGE ( 'NONE', *, *, #17603, .F. ) ;
#4597=DIRECTION ( 'NONE',  ( -1.000000000000000000, 0.000000000000000000, 0.000000000000000000 ) ) ;
#4669=DIRECTION ( 'NONE',  ( 0.000000000000000000, 1.000000000000000000, 0.000000000000000000 ) ) ;
#4717=AXIS2_PLACEMENT_3D ( 'NONE', #21526, #197, #7347 ) ;
#4751=EDGE_LOOP ( 'NONE', ( #5903, #17675, #8830, #18314 ) ) ;
#4755=CIRCLE ( 'NONE', #17461, 5.080000000000000071 ) ;
#4758=DIRECTION ( 'NONE',  ( 0.000000000000000000, 0.000000000000000000, 1.000000000000000000 ) ) ;
#4762=FACE_OUTER_BOUND ( 'NONE', #8178, .T. ) ;
#4768=LINE ( 'NONE', #10153, #2466 ) ;
#4773=DIRECTION ( 'NONE',  ( -0.8660254037825932949, 0.5000000000031962211, 0.000000000000000000 ) ) ;
#4776=CIRCLE ( 'NONE', #1394, 0.3809999999999647002 ) ;
#4783=EDGE_CURVE ( 'NONE', #3332, #7259, #5952, .T. ) ;
#4873=FACE_OUTER_BOUND ( 'NONE', #17189, .T. ) ;
#4999=PLANE ( 'NONE',  #10724 ) ;
#5016=DIRECTION ( 'NONE',  ( -0.8660254037827048723, 0.5000000000030029312, 0.000000000000000000 ) ) ;
#5085=CIRCLE ( 'NONE', #18175, 5.460999999999938126 ) ;
#5089=ORIENTED_EDGE ( 'NONE', *, *, #15995, .T. ) ;
#5192=CARTESIAN_POINT ( 'NONE',  ( 12.69999999996000106, -3642.194899999999961, 2292.781800000000203 ) ) ;
#5197=FACE_OUTER_BOUND ( 'NONE', #14238, .T. ) ;
#5306=DIRECTION ( 'NONE',  ( -0.5000000000040877302, 0.8660254037820785955, 0.000000000000000000 ) ) ;
#5309=CARTESIAN_POINT ( 'NONE',  ( 12.70000000023389042, -3642.634840905157944, 2296.591799999999694 ) ) ;
#5365=PRODUCT_DEFINITION ( 'UNKNOWN', '', #18354, #14646 ) ;
#5454=DIRECTION ( 'NONE',  ( 2.336881798971000105E-14, 2.336881798971000105E-14, 1.000000000000000000 ) ) ;
#5508=ORIENTED_EDGE ( 'NONE', *, *, #21772, .T. ) ;
#5609=DIRECTION ( 'NONE',  ( -2.848812946084999742E-12, -1.000000000000000000, 0.000000000000000000 ) ) ;
#5611=AXIS2_PLACEMENT_3D ( 'NONE', #2606, #9751, #7545 ) ;
#5636=DIRECTION ( 'NONE',  ( 0.000000000000000000, 0.000000000000000000, 1.000000000000000000 ) ) ;
#5651=CARTESIAN_POINT ( 'NONE',  ( 12.69999999996000106, -3642.194899999999961, 2292.781800000000203 ) ) ;
#5662=DIRECTION ( 'NONE',  ( 3.101153370604999976E-13, -3.885294924346999989E-13, -1.000000000000000000 ) ) ;
#5667=ORIENTED_EDGE ( 'NONE', *, *, #5945, .T. ) ;
#5683=DIRECTION ( 'NONE',  ( -5.461016542361937364E-28, 1.000000000000000000, -2.336881798971000105E-14 ) ) ;
#5687=EDGE_CURVE ( 'NONE', #22803, #11827, #6206, .T. ) ;
#5723=CARTESIAN_POINT ( 'NONE',  ( 12.69999999999999929, -3642.677500000000236, 2264.841800000000148 ) ) ;
#5831=AXIS2_PLACEMENT_3D ( 'NONE', #2387, #16668, #6480 ) ;
#5842=CARTESIAN_POINT ( 'NONE',  ( 17.78000000000000114, -3639.502500000000055, 2296.591799999999694 ) ) ;
#5903=ORIENTED_EDGE ( 'NONE', *, *, #81, .T. ) ;
#5915=AXIS2_PLACEMENT_3D ( 'NONE', #4181, #2091, #7818 ) ;
#5917=VECTOR ( 'NONE', #7182, 1000.000000000000114 ) ;
#5922=CARTESIAN_POINT ( 'NONE',  ( 12.69999999994000106, -3636.810100000000148, 2292.781800000000203 ) ) ;
#5926=VECTOR ( 'NONE', #12741, 1000.000000000000000 ) ;
#5945=EDGE_CURVE ( 'NONE', #14242, #16552, #4776, .T. ) ;
#5952=LINE ( 'NONE', #20351, #14992 ) ;
#5965=CYLINDRICAL_SURFACE ( 'NONE', #9552, 0.3809999999998115450 ) ;
#6016=EDGE_LOOP ( 'NONE', ( #2066, #22665 ) ) ;
#6018=EDGE_CURVE ( 'NONE', #2427, #15790, #4391, .T. ) ;
#6107=DIRECTION ( 'NONE',  ( 0.000000000000000000, 0.000000000000000000, 1.000000000000000000 ) ) ;
#6110=ORIENTED_EDGE ( 'NONE', *, *, #5687, .F. ) ;
#6126=EDGE_CURVE ( 'NONE', #2858, #16219, #768, .T. ) ;
#6187=CIRCLE ( 'NONE', #19646, 5.460999999999938126 ) ;
#6206=LINE ( 'NONE', #13345, #3995 ) ;
#6252=FACE_OUTER_BOUND ( 'NONE', #21703, .T. ) ;
#6262=DIRECTION ( 'NONE',  ( 0.000000000000000000, 2.336881798971000105E-14, 1.000000000000000000 ) ) ;
#6267=EDGE_CURVE ( 'NONE', #8402, #12177, #13715, .T. ) ;
#6331=ORIENTED_EDGE ( 'NONE', *, *, #8379, .F. ) ;
#6376=CARTESIAN_POINT ( 'NONE',  ( 12.69999999994000106, -3636.370159094999508, 2296.591799999999694 ) ) ;
#6388=DIRECTION ( 'NONE',  ( -1.000000000000000000, 1.206520773835000154E-12, 0.000000000000000000 ) ) ;
#6440=CARTESIAN_POINT ( 'NONE',  ( 15.41268679713999923, -3641.068670452857532, 2296.591799999999694 ) ) ;
#6480=DIRECTION ( 'NONE',  ( 0.000000000000000000, 1.000000000000000000, 0.000000000000000000 ) ) ;
#6508=DIRECTION ( 'NONE',  ( -2.336881798971000105E-14, 0.000000000000000000, -1.000000000000000000 ) ) ;
#6512=AXIS2_PLACEMENT_3D ( 'NONE', #7856, #6107, #4446 ) ;
#6513=CARTESIAN_POINT ( 'NONE',  ( 15.03168679706412902, -3638.156299999897783, 2296.210799999999836 ) ) ;
#6544=CARTESIAN_POINT ( 'NONE',  ( 7.619999999999999218, -3639.502500000000055, 2296.591799999999694 ) ) ;
#6586=EDGE_CURVE ( 'NONE', #13767, #7997, #8368, .T. ) ;
#6592=EDGE_CURVE ( 'NONE', #7259, #14462, #2730, .T. ) ;
#6593=AXIS2_PLACEMENT_3D ( 'NONE', #2670, #22351, #3139 ) ;
#6599=AXIS2_PLACEMENT_3D ( 'NONE', #1293, #8461, #10436 ) ;
#6659=DIRECTION ( 'NONE',  ( 0.000000000000000000, -1.000000000000000000, 0.000000000000000000 ) ) ;
#6690=ORIENTED_EDGE ( 'NONE', *, *, #15662, .F. ) ;
#6803=EDGE_CURVE ( 'NONE', #14462, #18372, #4236, .T. ) ;
#6859=DIRECTION ( 'NONE',  ( 0.000000000000000000, -1.000000000000000000, 0.000000000000000000 ) ) ;
#6875=VERTEX_POINT ( 'NONE', #16995 ) ;
#6883=DIRECTION ( 'NONE',  ( 0.000000000000000000, -1.000000000000000000, 0.000000000000000000 ) ) ;
#6889=CARTESIAN_POINT ( 'NONE',  ( 12.69999999999999929, -3639.502500000000055, 2263.571799999999712 ) ) ;
#6925=EDGE_CURVE ( 'NONE', #3332, #22999, #2595, .T. ) ;
#7004=EDGE_CURVE ( 'NONE', #17967, #2858, #7707, .T. ) ;
#7019=LINE ( 'NONE', #15559, #13186 ) ;
#7028=DIRECTION ( 'NONE',  ( -1.224646799141892071E-16, -1.000000000000000000, 2.336881798971000421E-14 ) ) ;
#7033=CIRCLE ( 'NONE', #23091, 1.269999999999882334 ) ;
#7036=ORIENTED_EDGE ( 'NONE', *, *, #13147, .F. ) ;
#7073=CARTESIAN_POINT ( 'NONE',  ( 12.69999999999133955, -3642.194900000167763, 2296.433984632682041 ) ) ;
#7092=EDGE_CURVE ( 'NONE', #14242, #2427, #5085, .T. ) ;
#7122=ADVANCED_FACE ( 'NONE', ( #13548, #4762 ), #4999, .T. ) ;
#7172=DIRECTION ( 'NONE',  ( 0.000000000000000000, 0.000000000000000000, -1.000000000000000000 ) ) ;
#7182=DIRECTION ( 'NONE',  ( 0.8660254037816071948, 0.5000000000049040771, 0.000000000000000000 ) ) ;
#7206=FACE_OUTER_BOUND ( 'NONE', #11626, .T. ) ;
#7243=VECTOR ( 'NONE', #18047, 999.9999999999998863 ) ;
#7259=VERTEX_POINT ( 'NONE', #17359 ) ;
#7272=CIRCLE ( 'NONE', #15890, 1.904999999999823501 ) ;
#7279=CARTESIAN_POINT ( 'NONE',  ( 7.238999999999998991, -3639.502500000000055, 2290.622800000000552 ) ) ;
#7347=DIRECTION ( 'NONE',  ( 0.000000000000000000, 1.000000000000000000, 0.000000000000000000 ) ) ;
#7371=CARTESIAN_POINT ( 'NONE',  ( 12.69999999999999929, -3639.502500000000055, 2263.571799999999712 ) ) ;
#7382=FACE_OUTER_BOUND ( 'NONE', #17505, .T. ) ;
#7396=VECTOR ( 'NONE', #15079, 1000.000000000000000 ) ;
#7409=( LENGTH_UNIT ( ) NAMED_UNIT ( * ) SI_UNIT ( .MILLI., .METRE. ) );
#7482=ORIENTED_EDGE ( 'NONE', *, *, #19024, .T. ) ;
#7500=CARTESIAN_POINT ( 'NONE',  ( 12.69999999999999929, -3639.502500000000055, 2296.210799999999836 ) ) ;
#7522=CARTESIAN_POINT ( 'NONE',  ( 12.69999999999999929, -3637.597499999999854, 2263.571799999999712 ) ) ;
#7544=CARTESIAN_POINT ( 'NONE',  ( 7.619999999999999218, -3639.502500000000055, 2290.622800000000097 ) ) ;
#7545=DIRECTION ( 'NONE',  ( 1.000000000000000000, 0.000000000000000000, 0.000000000000000000 ) ) ;
#7565=DIRECTION ( 'NONE',  ( 0.000000000000000000, -1.000000000000000000, 0.000000000000000000 ) ) ;
#7572=ADVANCED_FACE ( 'NONE', ( #17244 ), #3303, .T. ) ;
#7596=CARTESIAN_POINT ( 'NONE',  ( 12.69999999994000106, -3636.810100000000148, 2292.781800000000203 ) ) ;
#7626=( NAMED_UNIT ( * ) PLANE_ANGLE_UNIT ( ) SI_UNIT ( $, .RADIAN. ) );
#7693=DIRECTION ( 'NONE',  ( -7.280632624815000075E-13, -1.000000000000000000, -3.793660610169000352E-12 ) ) ;
#7707=CIRCLE ( 'NONE', #6599, 5.460999999999938126 ) ;
#7741=ORIENTED_EDGE ( 'NONE', *, *, #3342, .T. ) ;
#7797=CARTESIAN_POINT ( 'NONE',  ( 15.03168679714000078, -3638.156300000000101, 2292.781800000000203 ) ) ;
#7808=DIRECTION ( 'NONE',  ( 0.5000000000047110094, -0.8660254037817188832, 0.000000000000000000 ) ) ;
#7818=DIRECTION ( 'NONE',  ( 0.000000000000000000, -1.000000000000000000, 0.000000000000000000 ) ) ;
#7856=CARTESIAN_POINT ( 'NONE',  ( 12.69999999999999929, -3639.502500000000055, 2264.841800000000148 ) ) ;
#7858=VERTEX_POINT ( 'NONE', #16593 ) ;
#7861=( BOUNDED_CURVE ( )  B_SPLINE_CURVE ( 3, ( #6513, #20794, #10128, #18919 ),
 .UNSPECIFIED., .F., .T. ) 
 B_SPLINE_CURVE_WITH_KNOTS ( ( 4, 4 ),
 ( -2.664535259100375697E-14, 1.570796326277596799 ),
 .UNSPECIFIED. ) 
 CURVE ( )  GEOMETRIC_REPRESENTATION_ITEM ( )  RATIONAL_B_SPLINE_CURVE ( ( 1.000000000000000000, 0.8047378542462874096, 0.8047378542462874096, 1.000000000000000000 ) ) 
 REPRESENTATION_ITEM ( '' )  );
#7894=CARTESIAN_POINT ( 'NONE',  ( 12.69999999999999929, -3639.502500000000055, 2296.591799999999694 ) ) ;
#7930=CARTESIAN_POINT ( 'NONE',  ( 12.69999999999999929, -3644.963499999999840, 2290.241799999999785 ) ) ;
#7997=VERTEX_POINT ( 'NONE', #15299 ) ;
#8024=PLANE ( 'NONE',  #9520 ) ;
#8025=DIRECTION ( 'NONE',  ( 0.000000000000000000, 0.000000000000000000, 1.000000000000000000 ) ) ;
#8178=EDGE_LOOP ( 'NONE', ( #1226, #2847 ) ) ;
#8182=DIRECTION ( 'NONE',  ( 2.008939161382000013E-12, 1.000000000000000000, 3.793660610075000646E-12 ) ) ;
#8192=CARTESIAN_POINT ( 'NONE',  ( 11.34365660141000021, -3637.153244320999875, 2296.210799999999836 ) ) ;
#8214=CARTESIAN_POINT ( 'NONE',  ( 15.41268679701111566, -3637.936329547520472, 2296.591799999999694 ) ) ;
#8245=DIRECTION ( 'NONE',  ( -1.648694042066000049E-12, -1.000000000000000000, 0.000000000000000000 ) ) ;
#8280=ADVANCED_FACE ( 'NONE', ( #7206 ), #15228, .T. ) ;
#8308=FACE_OUTER_BOUND ( 'NONE', #17054, .T. ) ;
#8348=ORIENTED_EDGE ( 'NONE', *, *, #10587, .F. ) ;
#8368=LINE ( 'NONE', #1085, #11462 ) ;
#8379=EDGE_CURVE ( 'NONE', #16552, #2161, #4755, .T. ) ;
#8402=VERTEX_POINT ( 'NONE', #14930 ) ;
#8459=EDGE_LOOP ( 'NONE', ( #21239, #1133, #3466, #23089 ) ) ;
#8461=DIRECTION ( 'NONE',  ( -2.336881798971000105E-14, 0.000000000000000000, -1.000000000000000000 ) ) ;
#8511=AXIS2_PLACEMENT_3D ( 'NONE', #3280, #1163, #3157 ) ;
#8577=DIRECTION ( 'NONE',  ( 0.000000000000000000, 1.000000000000000000, 0.000000000000000000 ) ) ;
#8648=EDGE_CURVE ( 'NONE', #2498, #3774, #7033, .T. ) ;
#8672=FACE_OUTER_BOUND ( 'NONE', #4751, .T. ) ;
#8682=FACE_OUTER_BOUND ( 'NONE', #17763, .T. ) ;
#8690=AXIS2_PLACEMENT_3D ( 'NONE', #11213, #18243, #5609 ) ;
#8705=LINE ( 'NONE', #12684, #5917 ) ;
#8718=ORIENTED_EDGE ( 'NONE', *, *, #21851, .F. ) ;
#8719=ADVANCED_FACE ( 'NONE', ( #18068 ), #16078, .T. ) ;
#8777=DIRECTION ( 'NONE',  ( 0.8660254037820102058, 0.5000000000042060799, 0.000000000000000000 ) ) ;
#8784=ORIENTED_EDGE ( 'NONE', *, *, #9430, .T. ) ;
#8786=ORIENTED_EDGE ( 'NONE', *, *, #21726, .F. ) ;
#8797=CARTESIAN_POINT ( 'NONE',  ( 15.41268679713999923, -3641.068670452999868, 2296.591799999999694 ) ) ;
#8830=ORIENTED_EDGE ( 'NONE', *, *, #12662, .F. ) ;
#8856=CARTESIAN_POINT ( 'NONE',  ( 7.238999999999998991, -3639.502500000000055, 2296.210799999999836 ) ) ;
#8896=DIRECTION ( 'NONE',  ( -1.000000000000000000, 0.000000000000000000, 0.000000000000000000 ) ) ;
#8906=ORIENTED_EDGE ( 'NONE', *, *, #10143, .T. ) ;
#8913=CYLINDRICAL_SURFACE ( 'NONE', #3852, 0.3810000000000260956 ) ;
#8932=ADVANCED_FACE ( 'NONE', ( #19341 ), #1283, .T. ) ;
#8945=AXIS2_PLACEMENT_3D ( 'NONE', #13102, #2772, #2443 ) ;
#8958=CARTESIAN_POINT ( 'NONE',  ( 17.77999999999999758, -3639.502500000000055, 2290.241799999999785 ) ) ;
#9036=ORIENTED_EDGE ( 'NONE', *, *, #17741, .T. ) ;
#9043=DIRECTION ( 'NONE',  ( 0.000000000000000000, -2.336881798971000105E-14, -1.000000000000000000 ) ) ;
#9075=ADVANCED_FACE ( 'NONE', ( #7382 ), #21564, .T. ) ;
#9148=CIRCLE ( 'NONE', #22980, 5.460999999999938126 ) ;
#9171=ORIENTED_EDGE ( 'NONE', *, *, #9789, .T. ) ;
#9192=DIRECTION ( 'NONE',  ( 0.000000000000000000, 0.000000000000000000, 1.000000000000000000 ) ) ;
#9239=EDGE_CURVE ( 'NONE', #22803, #17848, #17191, .T. ) ;
#9277=CARTESIAN_POINT ( 'NONE',  ( 12.69999999996000106, -3642.194899999999961, 2292.781800000000203 ) ) ;
#9283=CARTESIAN_POINT ( 'NONE',  ( 12.69999999999999929, -3639.502500000000055, 2290.241799999999785 ) ) ;
#9311=ADVANCED_FACE ( 'NONE', ( #19656 ), #10022, .T. ) ;
#9341=ORIENTED_EDGE ( 'NONE', *, *, #2065, .T. ) ;
#9360=EDGE_CURVE ( 'NONE', #22999, #14462, #14163, .T. ) ;
#9363=CARTESIAN_POINT ( 'NONE',  ( 12.69999999997567208, -3642.194900000083180, 2296.210799999999836 ) ) ;
#9393=ORIENTED_EDGE ( 'NONE', *, *, #2691, .F. ) ;
#9430=EDGE_CURVE ( 'NONE', #2000, #8402, #20534, .T. ) ;
#9446=LINE ( 'NONE', #11200, #18166 ) ;
#9520=AXIS2_PLACEMENT_3D ( 'NONE', #21967, #16913, #2518 ) ;
#9549=FACE_OUTER_BOUND ( 'NONE', #21599, .T. ) ;
#9552=AXIS2_PLACEMENT_3D ( 'NONE', #2214, #2441, #17703 ) ;
#9625=AXIS2_PLACEMENT_3D ( 'NONE', #18183, #5306, #14674 ) ;
#9658=ADVANCED_FACE ( 'NONE', ( #5197 ), #12336, .F. ) ;
#9668=CARTESIAN_POINT ( 'NONE',  ( 10.36831320290272984, -3638.156299999887324, 2296.210799999999836 ) ) ;
#9670=CARTESIAN_POINT ( 'NONE',  ( 15.41268679713999923, -3641.068670452999868, 2296.591799999999694 ) ) ;
#9680=ORIENTED_EDGE ( 'NONE', *, *, #6803, .T. ) ;
#9715=FACE_OUTER_BOUND ( 'NONE', #22834, .T. ) ;
#9751=DIRECTION ( 'NONE',  ( 0.000000000000000000, 0.000000000000000000, 1.000000000000000000 ) ) ;
#9763=DIRECTION ( 'NONE',  ( -2.286657950257999976E-13, 0.000000000000000000, 1.000000000000000000 ) ) ;
#9764=EDGE_CURVE ( 'NONE', #2236, #22803, #14568, .T. ) ;
#9789=EDGE_CURVE ( 'NONE', #14462, #2024, #11041, .T. ) ;
#9792=DIRECTION ( 'NONE',  ( 2.336881798971000105E-14, 0.000000000000000000, 1.000000000000000000 ) ) ;
#9858=ORIENTED_EDGE ( 'NONE', *, *, #6586, .T. ) ;
#9876=AXIS2_PLACEMENT_3D ( 'NONE', #8192, #15337, #20846 ) ;
#10022=TOROIDAL_SURFACE ( 'NONE', #19377, 5.080000000000000071, 0.3810000000000000053 ) ;
#10023=ORIENTED_EDGE ( 'NONE', *, *, #6018, .F. ) ;
#10091=ORIENTED_EDGE ( 'NONE', *, *, #11994, .F. ) ;
#10128=CARTESIAN_POINT ( 'NONE',  ( 15.18950216430036981, -3638.065185255141387, 2296.591799999884188 ) ) ;
#10143=EDGE_CURVE ( 'NONE', #12177, #8402, #11808, .T. ) ;
#10153=CARTESIAN_POINT ( 'NONE',  ( 10.36831320283000046, -3640.848700000000008, 2296.210799999999836 ) ) ;
#10176=DIRECTION ( 'NONE',  ( 0.000000000000000000, -2.336881798971000105E-14, -1.000000000000000000 ) ) ;
#10178=CARTESIAN_POINT ( 'NONE',  ( 10.36831320284000135, -3638.156300000000101, 2296.210799999999836 ) ) ;
#10260=EDGE_CURVE ( 'NONE', #16631, #2427, #21198, .T. ) ;
#10262=DIRECTION ( 'NONE',  ( 2.336881798971000105E-14, 2.336881798971000105E-14, 1.000000000000000000 ) ) ;
#10347=CARTESIAN_POINT ( 'NONE',  ( 15.03168679713838074, -3640.848700000155077, 2296.433984632765259 ) ) ;
#10362=ORIENTED_EDGE ( 'NONE', *, *, #5945, .F. ) ;
#10372=CARTESIAN_POINT ( 'NONE',  ( 9.987313202835000681, -3637.936329547143941, 2296.591799999999694 ) ) ;
#10374=AXIS2_PLACEMENT_3D ( 'NONE', #16395, #10775, #21332 ) ;
#10389=CARTESIAN_POINT ( 'NONE',  ( 12.69999999997316742, -3636.627870510297726, 2296.591799999996965 ) ) ;
#10419=EDGE_CURVE ( 'NONE', #16631, #17967, #11440, .T. ) ;
#10436=DIRECTION ( 'NONE',  ( 0.000000000000000000, -1.000000000000000000, 0.000000000000000000 ) ) ;
#10501=PRODUCT ( 'Screw 6', 'Screw 6', '', ( #13893 ) ) ;
#10531=LINE ( 'NONE', #19327, #14059 ) ;
#10565=EDGE_LOOP ( 'NONE', ( #16781, #18235, #8786, #808 ) ) ;
#10566=AXIS2_PLACEMENT_3D ( 'NONE', #21330, #3041, #19452 ) ;
#10581=DIRECTION ( 'NONE',  ( -1.000000000000000000, 0.000000000000000000, -2.902585187577999742E-13 ) ) ;
#10587=EDGE_CURVE ( 'NONE', #19668, #257, #3989, .T. ) ;
#10699=VECTOR ( 'NONE', #12288, 1000.000000000000000 ) ;
#10724=AXIS2_PLACEMENT_3D ( 'NONE', #11909, #10262, #15198 ) ;
#10768=DIRECTION ( 'NONE',  ( 0.000000000000000000, -1.000000000000000000, 0.000000000000000000 ) ) ;
#10775=DIRECTION ( 'NONE',  ( 2.848812946084999742E-12, 1.000000000000000000, -2.336881798978000141E-14 ) ) ;
#10844=CARTESIAN_POINT ( 'NONE',  ( 17.78000000000000114, -3639.502500000000055, 2290.622800000000097 ) ) ;
#10868=ADVANCED_FACE ( 'NONE', ( #9715 ), #18206, .T. ) ;
#10906=ORIENTED_EDGE ( 'NONE', *, *, #910, .T. ) ;
#10977=ORIENTED_EDGE ( 'NONE', *, *, #2664, .F. ) ;
#11041=LINE ( 'NONE', #16202, #14538 ) ;
#11150=VECTOR ( 'NONE', #8182, 1000.000000000000000 ) ;
#11167=ORIENTED_EDGE ( 'NONE', *, *, #21618, .T. ) ;
#11200=CARTESIAN_POINT ( 'NONE',  ( 15.03168679714000078, -3638.156300000000101, 2292.781800000000203 ) ) ;
#11204=PLANE ( 'NONE',  #20677 ) ;
#11213=CARTESIAN_POINT ( 'NONE',  ( 10.36831320283000046, -3640.848700000000008, 2292.781800000000203 ) ) ;
#11269=CARTESIAN_POINT ( 'NONE',  ( 10.36831320283000046, -3640.848700000000008, 2296.210799999999836 ) ) ;
#11335=FACE_OUTER_BOUND ( 'NONE', #14224, .T. ) ;
#11401=DIRECTION ( 'NONE',  ( 7.082568872520999671E-14, 2.590196616236000185E-13, 1.000000000000000000 ) ) ;
#11440=CIRCLE ( 'NONE', #11828, 5.460999999999938126 ) ;
#11453=PLANE ( 'NONE',  #8945 ) ;
#11462=VECTOR ( 'NONE', #8245, 1000.000000000000000 ) ;
#11562=CARTESIAN_POINT ( 'NONE',  ( 12.69999999999999929, -3642.677500000000236, 2264.841800000000148 ) ) ;
#11626=EDGE_LOOP ( 'NONE', ( #10362, #1769, #17510, #17339, #6331 ) ) ;
#11654=ADVANCED_FACE ( 'NONE', ( #17029 ), #8024, .T. ) ;
#11694=DIRECTION ( 'NONE',  ( 0.000000000000000000, 0.000000000000000000, -1.000000000000000000 ) ) ;
#11700=VECTOR ( 'NONE', #18722, 1000.000000000000000 ) ;
#11808=CIRCLE ( 'NONE', #6593, 3.175000000000149925 ) ;
#11817=CYLINDRICAL_SURFACE ( 'NONE', #9876, 0.3809999999999303388 ) ;
#11827=VERTEX_POINT ( 'NONE', #9277 ) ;
#11828=AXIS2_PLACEMENT_3D ( 'NONE', #21424, #95, #14167 ) ;
#11909=CARTESIAN_POINT ( 'NONE',  ( 12.69999999999999929, -3639.502500000000055, 2296.591799999999694 ) ) ;
#11994=EDGE_CURVE ( 'NONE', #671, #204, #1038, .T. ) ;
#12012=APPLICATION_CONTEXT ( 'configuration controlled 3d designs of mechanical parts and assemblies' ) ;
#12052=CIRCLE ( 'NONE', #3823, 0.3809999999999647002 ) ;
#12088=ORIENTED_EDGE ( 'NONE', *, *, #17741, .F. ) ;
#12119=ORIENTED_EDGE ( 'NONE', *, *, #15662, .T. ) ;
#12124=ORIENTED_EDGE ( 'NONE', *, *, #12607, .F. ) ;
#12138=DIRECTION ( 'NONE',  ( 2.336881798971000105E-14, 2.336881798971000105E-14, 1.000000000000000000 ) ) ;
#12177=VERTEX_POINT ( 'NONE', #12410 ) ;
#12227=AXIS2_PLACEMENT_3D ( 'NONE', #17640, #19177, #6883 ) ;
#12253=EDGE_CURVE ( 'NONE', #2858, #257, #6187, .T. ) ;
#12275=FACE_OUTER_BOUND ( 'NONE', #19162, .T. ) ;
#12278=ORIENTED_EDGE ( 'NONE', *, *, #10260, .T. ) ;
#12288=DIRECTION ( 'NONE',  ( 0.000000000000000000, 0.000000000000000000, 1.000000000000000000 ) ) ;
#12289=DIRECTION ( 'NONE',  ( 0.000000000000000000, 0.000000000000000000, -1.000000000000000000 ) ) ;
#12296=CARTESIAN_POINT ( 'NONE',  ( 12.69999999999999929, -3639.502500000000055, 2290.622800000000097 ) ) ;
#12336=PLANE ( 'NONE',  #13781 ) ;
#12391=ORIENTED_EDGE ( 'NONE', *, *, #3342, .F. ) ;
#12410=CARTESIAN_POINT ( 'NONE',  ( 12.69999999999999929, -3636.327499999999873, 2290.241799999999785 ) ) ;
#12451=CARTESIAN_POINT ( 'NONE',  ( 12.69999999999143903, -3642.377129489641902, 2296.591799999931936 ) ) ;
#12479=ORIENTED_EDGE ( 'NONE', *, *, #21772, .F. ) ;
#12544=LINE ( 'NONE', #8797, #7243 ) ;
#12582=ORIENTED_EDGE ( 'NONE', *, *, #6126, .T. ) ;
#12584=ORIENTED_EDGE ( 'NONE', *, *, #7004, .F. ) ;
#12589=CIRCLE ( 'NONE', #4717, 3.175000000000149925 ) ;
#12607=EDGE_CURVE ( 'NONE', #15790, #16219, #9148, .T. ) ;
#12662=EDGE_CURVE ( 'NONE', #3774, #6875, #7272, .T. ) ;
#12684=CARTESIAN_POINT ( 'NONE',  ( 9.987313202835000681, -3637.936329547000241, 2296.591799999999694 ) ) ;
#12728=CARTESIAN_POINT ( 'NONE',  ( 12.69999999999999929, -3639.502500000000055, 2264.841800000000148 ) ) ;
#12740=( GEOMETRIC_REPRESENTATION_CONTEXT ( 3 ) GLOBAL_UNCERTAINTY_ASSIGNED_CONTEXT ( ( #2448 ) ) GLOBAL_UNIT_ASSIGNED_CONTEXT ( ( #7409, #7626, #20287 ) ) REPRESENTATION_CONTEXT ( 'NONE', 'WORKASPACE' ) );
#12741=DIRECTION ( 'NONE',  ( -1.297627797025000031E-12, -1.000000000000000000, 0.000000000000000000 ) ) ;
#12771=DIRECTION ( 'NONE',  ( 0.000000000000000000, -1.000000000000000000, 0.000000000000000000 ) ) ;
#12792=DIRECTION ( 'NONE',  ( -1.000000000000000000, 0.000000000000000000, 0.000000000000000000 ) ) ;
#12857=DIRECTION ( 'NONE',  ( -5.461016542361937364E-28, 1.000000000000000000, -2.336881798971000105E-14 ) ) ;
#12863=ADVANCED_FACE ( 'NONE', ( #3587 ), #1834, .T. ) ;
#12893=ORIENTED_EDGE ( 'NONE', *, *, #12662, .T. ) ;
#12919=ORIENTED_EDGE ( 'NONE', *, *, #9239, .T. ) ;
#12976=PLANE ( 'NONE',  #8690 ) ;
#13043=VECTOR ( 'NONE', #5662, 1000.000000000000000 ) ;
#13046=DIRECTION ( 'NONE',  ( 1.000000000000000000, -1.165588477296748772E-12, 0.000000000000000000 ) ) ;
#13069=ORIENTED_EDGE ( 'NONE', *, *, #10260, .F. ) ;
#13102=CARTESIAN_POINT ( 'NONE',  ( 12.69999999999999929, -3639.502500000000055, 2290.241799999999785 ) ) ;
#13117=CARTESIAN_POINT ( 'NONE',  ( 10.36831320282916202, -3640.848700000148256, 2296.433984632680676 ) ) ;
#13147=EDGE_CURVE ( 'NONE', #257, #16631, #15906, .T. ) ;
#13186=VECTOR ( 'NONE', #5016, 1000.000000000000114 ) ;
#13194=EDGE_LOOP ( 'NONE', ( #12893, #21773 ) ) ;
#13218=ORIENTED_EDGE ( 'NONE', *, *, #3717, .F. ) ;
#13261=CYLINDRICAL_SURFACE ( 'NONE', #15159, 0.3810000000000011156 ) ;
#13306=ORIENTED_EDGE ( 'NONE', *, *, #2691, .T. ) ;
#13345=CARTESIAN_POINT ( 'NONE',  ( 10.36831320283000046, -3640.848700000000008, 2292.781800000000203 ) ) ;
#13346=LINE ( 'NONE', #1027, #11700 ) ;
#13470=VERTEX_POINT ( 'NONE', #18543 ) ;
#13501=EDGE_CURVE ( 'NONE', #2000, #6875, #2076, .T. ) ;
#13548=FACE_BOUND ( 'NONE', #22873, .T. ) ;
#13580=CARTESIAN_POINT ( 'NONE',  ( 10.36831320284000135, -3638.156300000000101, 2292.781800000000203 ) ) ;
#13620=DIRECTION ( 'NONE',  ( 0.5000000000031962211, 0.8660254037825932949, 0.000000000000000000 ) ) ;
#13658=CARTESIAN_POINT ( 'NONE',  ( 10.36831320290272984, -3638.156299999887324, 2296.210799999999836 ) ) ;
#13663=CARTESIAN_POINT ( 'NONE',  ( 12.69999999999999929, -3639.502500000000055, 2290.241799999999785 ) ) ;
#13710=ORIENTED_EDGE ( 'NONE', *, *, #19872, .T. ) ;
#13715=CIRCLE ( 'NONE', #15955, 3.175000000000149925 ) ;
#13720=CIRCLE ( 'NONE', #12227, 5.460999999999938126 ) ;
#13767=VERTEX_POINT ( 'NONE', #14207 ) ;
#13781=AXIS2_PLACEMENT_3D ( 'NONE', #1667, #15856, #10581 ) ;
#13791=CARTESIAN_POINT ( 'NONE',  ( 15.03168679714000078, -3638.156300000000101, 2292.781800000000203 ) ) ;
#13801=LINE ( 'NONE', #18830, #14327 ) ;
#13833=ORIENTED_EDGE ( 'NONE', *, *, #17603, .T. ) ;
#13893=PRODUCT_CONTEXT ( 'NONE', #12012, 'mechanical' ) ;
#13945=ORIENTED_EDGE ( 'NONE', *, *, #19024, .F. ) ;
#13968=CIRCLE ( 'NONE', #19571, 5.080000000000000959 ) ;
#13985=TOROIDAL_SURFACE ( 'NONE', #10566, 1.905000000000000027, 1.270000000000000018 ) ;
#14018=ORIENTED_EDGE ( 'NONE', *, *, #10587, .T. ) ;
#14049=CARTESIAN_POINT ( 'NONE',  ( 18.16100000000000136, -3639.502500000000055, 2290.622800000000097 ) ) ;
#14054=CYLINDRICAL_SURFACE ( 'NONE', #19662, 5.460999999999938126 ) ;
#14059=VECTOR ( 'NONE', #8777, 1000.000000000000114 ) ;
#14163=LINE ( 'NONE', #21652, #5926 ) ;
#14167=DIRECTION ( 'NONE',  ( 0.000000000000000000, -1.000000000000000000, 0.000000000000000000 ) ) ;
#14178=DIRECTION ( 'NONE',  ( 2.336881798971000105E-14, 2.336881798971000105E-14, 1.000000000000000000 ) ) ;
#14207=CARTESIAN_POINT ( 'NONE',  ( 9.987313202835000681, -3637.936329547143941, 2296.591799999999694 ) ) ;
#14224=EDGE_LOOP ( 'NONE', ( #9171, #17346, #22265, #19399 ) ) ;
#14238=EDGE_LOOP ( 'NONE', ( #19753, #13710, #2653, #15860, #10906, #16039 ) ) ;
#14242=VERTEX_POINT ( 'NONE', #3216 ) ;
#14254=AXIS2_PLACEMENT_3D ( 'NONE', #5192, #13620, #20767 ) ;
#14275=DIRECTION ( 'NONE',  ( 2.336881798971000105E-14, 2.336881798971000105E-14, 1.000000000000000000 ) ) ;
#14327=VECTOR ( 'NONE', #4773, 1000.000000000000000 ) ;
#14368=ORIENTED_EDGE ( 'NONE', *, *, #6925, .F. ) ;
#14423=DIRECTION ( 'NONE',  ( -0.8660254037825932949, 0.5000000000031962211, 0.000000000000000000 ) ) ;
#14462=VERTEX_POINT ( 'NONE', #18771 ) ;
#14467=CARTESIAN_POINT ( 'NONE',  ( 12.69999999994000106, -3636.810100000000148, 2292.781800000000203 ) ) ;
#14513=FACE_OUTER_BOUND ( 'NONE', #1424, .T. ) ;
#14538=VECTOR ( 'NONE', #18188, 1000.000000000000000 ) ;
#14568=LINE ( 'NONE', #11269, #13043 ) ;
#14646=PRODUCT_DEFINITION_CONTEXT ( 'detailed design', #15302, 'design' ) ;
#14658=DIRECTION ( 'NONE',  ( 0.000000000000000000, -1.000000000000000000, 0.000000000000000000 ) ) ;
#14674=DIRECTION ( 'NONE',  ( 0.000000000000000000, 0.000000000000000000, 1.000000000000000000 ) ) ;
#14774=ORIENTED_EDGE ( 'NONE', *, *, #9360, .T. ) ;
#14787=SHAPE_REPRESENTATION_RELATIONSHIP ( 'NONE' , 'NONE' ,  #19840, #1231 ) ;
#14849=DIRECTION ( 'NONE',  ( 0.000000000000000000, 0.000000000000000000, -1.000000000000000000 ) ) ;
#14930=CARTESIAN_POINT ( 'NONE',  ( 12.69999999999981988, -3642.677500000000236, 2290.241799999999785 ) ) ;
#14940=ADVANCED_FACE ( 'NONE', ( #8672 ), #13985, .T. ) ;
#14948=ORIENTED_EDGE ( 'NONE', *, *, #15896, .T. ) ;
#14969=ORIENTED_EDGE ( 'NONE', *, *, #3643, .F. ) ;
#14978=ORIENTED_EDGE ( 'NONE', *, *, #17557, .T. ) ;
#14992=VECTOR ( 'NONE', #7693, 1000.000000000000000 ) ;
#15004=FACE_OUTER_BOUND ( 'NONE', #3906, .T. ) ;
#15012=ORIENTED_EDGE ( 'NONE', *, *, #3717, .T. ) ;
#15013=CARTESIAN_POINT ( 'NONE',  ( 12.69999999999999929, -3636.327499999999873, 2264.841800000000148 ) ) ;
#15079=DIRECTION ( 'NONE',  ( 0.000000000000000000, 0.000000000000000000, 1.000000000000000000 ) ) ;
#15159=AXIS2_PLACEMENT_3D ( 'NONE', #20416, #20522, #13046 ) ;
#15169=ORIENTED_EDGE ( 'NONE', *, *, #8648, .T. ) ;
#15198=DIRECTION ( 'NONE',  ( 1.000000000000000000, 0.000000000000000000, -2.336881798971000105E-14 ) ) ;
#15228=TOROIDAL_SURFACE ( 'NONE', #23077, 5.080000000000000071, 0.3810000000000000053 ) ;
#15299=CARTESIAN_POINT ( 'NONE',  ( 9.987313202947046165, -3641.068670452640163, 2296.591799999999694 ) ) ;
#15302=APPLICATION_CONTEXT ( 'configuration controlled 3d designs of mechanical parts and assemblies' ) ;
#15305=EDGE_CURVE ( 'NONE', #13470, #7997, #7019, .T. ) ;
#15337=DIRECTION ( 'NONE',  ( 0.8660254037817188832, 0.5000000000047110094, -3.192239903041070306E-14 ) ) ;
#15396=CARTESIAN_POINT ( 'NONE',  ( 15.03168679714000078, -3640.848700000000008, 2292.781800000000203 ) ) ;
#15493=ORIENTED_EDGE ( 'NONE', *, *, #10419, .F. ) ;
#15559=CARTESIAN_POINT ( 'NONE',  ( 12.69999999996000106, -3642.634840905000146, 2296.591799999999694 ) ) ;
#15561=ORIENTED_EDGE ( 'NONE', *, *, #15995, .F. ) ;
#15570=CARTESIAN_POINT ( 'NONE',  ( 12.69999999999999929, -3634.041499999999814, 2290.241799999999785 ) ) ;
#15662=EDGE_CURVE ( 'NONE', #13767, #671, #19080, .T. ) ;
#15670=CARTESIAN_POINT ( 'NONE',  ( 12.69999999999999929, -3639.502500000000055, 2296.210799999999836 ) ) ;
#15790=VERTEX_POINT ( 'NONE', #8856 ) ;
#15856=DIRECTION ( 'NONE',  ( 2.902585187577999742E-13, 4.457650181899999573E-12, -1.000000000000000000 ) ) ;
#15860=ORIENTED_EDGE ( 'NONE', *, *, #21726, .T. ) ;
#15890=AXIS2_PLACEMENT_3D ( 'NONE', #6889, #17765, #21060 ) ;
#15896=EDGE_CURVE ( 'NONE', #22386, #204, #4485, .T. ) ;
#15906=CIRCLE ( 'NONE', #22236, 5.460999999999938126 ) ;
#15937=( BOUNDED_CURVE ( )  B_SPLINE_CURVE ( 3, ( #3242, #10389, #19529, #3468 ),
 .UNSPECIFIED., .F., .T. ) 
 B_SPLINE_CURVE_WITH_KNOTS ( ( 4, 4 ),
 ( 1.570796326807037513, 3.141592653589829975 ),
 .UNSPECIFIED. ) 
 CURVE ( )  GEOMETRIC_REPRESENTATION_ITEM ( )  RATIONAL_B_SPLINE_CURVE ( ( 1.000000000000000000, 0.8047378541272178776, 0.8047378541272178776, 1.000000000000000000 ) ) 
 REPRESENTATION_ITEM ( '' )  );
#15955=AXIS2_PLACEMENT_3D ( 'NONE', #13663, #4758, #17169 ) ;
#15971=VECTOR ( 'NONE', #9763, 1000.000000000000000 ) ;
#15995=EDGE_CURVE ( 'NONE', #7858, #4050, #22635, .T. ) ;
#16005=EDGE_LOOP ( 'NONE', ( #15493, #12278, #21429, #12391, #20334, #12584 ) ) ;
#16039=ORIENTED_EDGE ( 'NONE', *, *, #9239, .F. ) ;
#16042=CARTESIAN_POINT ( 'NONE',  ( 12.69999999999999929, -3639.502500000000055, 2296.591799999999694 ) ) ;
#16078=PLANE ( 'NONE',  #9625 ) ;
#16197=DIRECTION ( 'NONE',  ( 0.000000000000000000, 0.000000000000000000, 1.000000000000000000 ) ) ;
#16202=CARTESIAN_POINT ( 'NONE',  ( 15.03168679714000078, -3640.848700000000008, 2296.210799999999836 ) ) ;
#16219=VERTEX_POINT ( 'NONE', #19371 ) ;
#16225=AXIS2_PLACEMENT_3D ( 'NONE', #22850, #17582, #8577 ) ;
#16256=CARTESIAN_POINT ( 'NONE',  ( 12.69999999999999929, -3639.502500000000055, 2290.622800000000097 ) ) ;
#16376=CARTESIAN_POINT ( 'NONE',  ( 7.619999999999999218, -3639.502500000000055, 2296.210799999999836 ) ) ;
#16395=CARTESIAN_POINT ( 'NONE',  ( 9.987313202833000503, -3639.502500000000055, 2296.210799999999836 ) ) ;
#16552=VERTEX_POINT ( 'NONE', #5842 ) ;
#16588=EDGE_CURVE ( 'NONE', #15790, #2161, #12052, .T. ) ;
#16593=CARTESIAN_POINT ( 'NONE',  ( 12.69999999997255280, -3636.370159094721657, 2296.591799999999694 ) ) ;
#16602=ADVANCED_FACE ( 'NONE', ( #14513 ), #12976, .T. ) ;
#16631=VERTEX_POINT ( 'NONE', #3712 ) ;
#16668=DIRECTION ( 'NONE',  ( 1.000000000000000000, 1.224646799147353207E-16, 0.000000000000000000 ) ) ;
#16741=UNCERTAINTY_MEASURE_WITH_UNIT (LENGTH_MEASURE( 1.000000000000000082E-05 ), #21126, 'distance_accuracy_value', 'NONE');
#16760=EDGE_LOOP ( 'NONE', ( #2048, #21734, #15561, #11167 ) ) ;
#16781=ORIENTED_EDGE ( 'NONE', *, *, #20807, .F. ) ;
#16805=ORIENTED_EDGE ( 'NONE', *, *, #15305, .T. ) ;
#16913=DIRECTION ( 'NONE',  ( -0.5000000000005969669, -0.8660254037840939834, 0.000000000000000000 ) ) ;
#16995=CARTESIAN_POINT ( 'NONE',  ( 12.69999999999999929, -3641.407499999999800, 2263.571799999999712 ) ) ;
#16998=ORIENTED_EDGE ( 'NONE', *, *, #16588, .F. ) ;
#17029=FACE_OUTER_BOUND ( 'NONE', #10565, .T. ) ;
#17048=VECTOR ( 'NONE', #22310, 1000.000000000000000 ) ;
#17054=EDGE_LOOP ( 'NONE', ( #13218, #12119, #21109, #20060 ) ) ;
#17122=ORIENTED_EDGE ( 'NONE', *, *, #6267, .T. ) ;
#17169=DIRECTION ( 'NONE',  ( -5.682243826821398966E-14, -1.000000000000000000, 0.000000000000000000 ) ) ;
#17189=EDGE_LOOP ( 'NONE', ( #3727, #7741, #5667, #20382, #16998 ) ) ;
#17191=LINE ( 'NONE', #19314, #11150 ) ;
#17244=FACE_OUTER_BOUND ( 'NONE', #19280, .T. ) ;
#17296=DIRECTION ( 'NONE',  ( 2.822694825533999934E-12, 1.000000000000000000, 0.000000000000000000 ) ) ;
#17303=ORIENTED_EDGE ( 'NONE', *, *, #910, .F. ) ;
#17316=VECTOR ( 'NONE', #3757, 1000.000000000000000 ) ;
#17339=ORIENTED_EDGE ( 'NONE', *, *, #16588, .T. ) ;
#17346=ORIENTED_EDGE ( 'NONE', *, *, #3643, .T. ) ;
#17359=CARTESIAN_POINT ( 'NONE',  ( 15.03168679714000078, -3640.848700000000008, 2292.781800000000203 ) ) ;
#17438=DIRECTION ( 'NONE',  ( -1.000000000000000000, 5.461016542361937364E-28, 2.336881798970999789E-14 ) ) ;
#17443=ADVANCED_FACE ( 'NONE', ( #21339 ), #8913, .T. ) ;
#17461=AXIS2_PLACEMENT_3D ( 'NONE', #7894, #6262, #4597 ) ;
#17487=DIRECTION ( 'NONE',  ( 0.8660254037838025498, -0.5000000000011017853, 0.000000000000000000 ) ) ;
#17494=CARTESIAN_POINT ( 'NONE',  ( 15.18950216443630374, -3640.939814744946034, 2296.591800000036528 ) ) ;
#17505=EDGE_LOOP ( 'NONE', ( #9858, #13833, #21205, #6690 ) ) ;
#17510=ORIENTED_EDGE ( 'NONE', *, *, #6018, .T. ) ;
#17521=DIRECTION ( 'NONE',  ( -1.000000000000000000, 5.461016542361937364E-28, 2.336881798970999789E-14 ) ) ;
#17552=CARTESIAN_POINT ( 'NONE',  ( 12.69999999999999929, -3639.502500000000055, 2290.241799999999785 ) ) ;
#17557=EDGE_CURVE ( 'NONE', #18372, #13470, #12544, .T. ) ;
#17572=ADVANCED_FACE ( 'NONE', ( #8682 ), #21680, .T. ) ;
#17582=DIRECTION ( 'NONE',  ( 0.000000000000000000, 0.000000000000000000, -1.000000000000000000 ) ) ;
#17603=EDGE_CURVE ( 'NONE', #7997, #2236, #2189, .T. ) ;
#17621=EDGE_LOOP ( 'NONE', ( #10977, #7482, #23064, #778, #8348 ) ) ;
#17637=AXIS2_PLACEMENT_3D ( 'NONE', #3523, #7172, #21807 ) ;
#17640=CARTESIAN_POINT ( 'NONE',  ( 12.69999999999999929, -3639.502500000000055, 2296.210799999999836 ) ) ;
#17671=DIRECTION ( 'NONE',  ( 0.000000000000000000, 2.336881798971000105E-14, 1.000000000000000000 ) ) ;
#17675=ORIENTED_EDGE ( 'NONE', *, *, #13501, .T. ) ;
#17703=DIRECTION ( 'NONE',  ( 0.5000000000043351989, -0.8660254037819355988, 0.000000000000000000 ) ) ;
#17741=EDGE_CURVE ( 'NONE', #17848, #671, #13346, .T. ) ;
#17749=TOROIDAL_SURFACE ( 'NONE', #20023, 5.080000000000000071, 0.3810000000000000053 ) ;
#17763=EDGE_LOOP ( 'NONE', ( #13069, #7036, #3560, #12582, #12124, #10023 ) ) ;
#17765=DIRECTION ( 'NONE',  ( 0.000000000000000000, 0.000000000000000000, -1.000000000000000000 ) ) ;
#17848=VERTEX_POINT ( 'NONE', #13580 ) ;
#17946=EDGE_LOOP ( 'NONE', ( #2820, #3537, #22078, #13306 ) ) ;
#17967=VERTEX_POINT ( 'NONE', #14049 ) ;
#17978=DIRECTION ( 'NONE',  ( -1.000000000000000000, 5.461016542361937364E-28, 2.336881798970999789E-14 ) ) ;
#18019=CARTESIAN_POINT ( 'NONE',  ( 17.78000000000000114, -3639.502500000000055, 2296.210799999999836 ) ) ;
#18047=DIRECTION ( 'NONE',  ( -0.8660254037820787065, -0.5000000000040877302, 0.000000000000000000 ) ) ;
#18068=FACE_OUTER_BOUND ( 'NONE', #17946, .T. ) ;
#18158=CARTESIAN_POINT ( 'NONE',  ( 10.21049783562821034, -3640.939814744883734, 2296.591799999930572 ) ) ;
#18166=VECTOR ( 'NONE', #4166, 1000.000000000000114 ) ;
#18169=AXIS2_PLACEMENT_3D ( 'NONE', #12296, #14178, #17438 ) ;
#18175=AXIS2_PLACEMENT_3D ( 'NONE', #7500, #9792, #14658 ) ;
#18183=CARTESIAN_POINT ( 'NONE',  ( 15.03168679714000078, -3640.848700000000008, 2292.781800000000203 ) ) ;
#18188=DIRECTION ( 'NONE',  ( -0.8660254037821217832, -0.5000000000040129011, 0.000000000000000000 ) ) ;
#18206=TOROIDAL_SURFACE ( 'NONE', #1737, 1.905000000000000027, 1.270000000000000018 ) ;
#18235=ORIENTED_EDGE ( 'NONE', *, *, #15896, .F. ) ;
#18243=DIRECTION ( 'NONE',  ( 1.000000000000000000, -2.848812946084999742E-12, 0.000000000000000000 ) ) ;
#18273=CARTESIAN_POINT ( 'NONE',  ( 9.987313202947046165, -3641.068670452640163, 2296.591799999999694 ) ) ;
#18314=ORIENTED_EDGE ( 'NONE', *, *, #8648, .F. ) ;
#18354=PRODUCT_DEFINITION_FORMATION_WITH_SPECIFIED_SOURCE ( 'ANY', '', #10501, .NOT_KNOWN. ) ;
#18365=FACE_OUTER_BOUND ( 'NONE', #13194, .T. ) ;
#18371=ADVANCED_FACE ( 'NONE', ( #8308 ), #11817, .T. ) ;
#18372=VERTEX_POINT ( 'NONE', #6440 ) ;
#18539=ORIENTED_EDGE ( 'NONE', *, *, #21400, .F. ) ;
#18543=CARTESIAN_POINT ( 'NONE',  ( 12.70000000023389042, -3642.634840905157944, 2296.591799999999694 ) ) ;
#18635=CARTESIAN_POINT ( 'NONE',  ( 12.69999999999999929, -3644.963499999999840, 2290.622800000000097 ) ) ;
#18722=DIRECTION ( 'NONE',  ( 3.283276570194000329E-13, 2.590196616239000129E-13, 1.000000000000000000 ) ) ;
#18771=CARTESIAN_POINT ( 'NONE',  ( 15.03168679707239441, -3640.848700000039116, 2296.210799999999836 ) ) ;
#18812=ORIENTED_EDGE ( 'NONE', *, *, #2065, .F. ) ;
#18830=CARTESIAN_POINT ( 'NONE',  ( 12.69999999996000106, -3642.194899999999961, 2296.210799999999836 ) ) ;
#18902=VECTOR ( 'NONE', #22476, 1000.000000000000000 ) ;
#18911=ORIENTED_EDGE ( 'NONE', *, *, #15305, .F. ) ;
#18915=AXIS2_PLACEMENT_3D ( 'NONE', #16042, #17671, #8896 ) ;
#18919=CARTESIAN_POINT ( 'NONE',  ( 15.41268679701111566, -3637.936329547520472, 2296.591799999999694 ) ) ;
#18956=ADVANCED_FACE ( 'NONE', ( #4873 ), #17749, .T. ) ;
#18978=ORIENTED_EDGE ( 'NONE', *, *, #6586, .F. ) ;
#19024=EDGE_CURVE ( 'NONE', #22154, #17967, #20743, .T. ) ;
#19042=CARTESIAN_POINT ( 'NONE',  ( 15.03168679706412902, -3638.156299999897783, 2296.210799999999836 ) ) ;
#19080=( BOUNDED_CURVE ( )  B_SPLINE_CURVE ( 3, ( #10372, #22552, #22669, #13658 ),
 .UNSPECIFIED., .F., .T. ) 
 B_SPLINE_CURVE_WITH_KNOTS ( ( 4, 4 ),
 ( 1.570796326625032657, 3.141592653589783346 ),
 .UNSPECIFIED. ) 
 CURVE ( )  GEOMETRIC_REPRESENTATION_ITEM ( )  RATIONAL_B_SPLINE_CURVE ( ( 1.000000000000000000, 0.8047378540843299621, 0.8047378540843299621, 1.000000000000000000 ) ) 
 REPRESENTATION_ITEM ( '' )  );
#19162=EDGE_LOOP ( 'NONE', ( #10091, #12088, #17303, #14948 ) ) ;
#19177=DIRECTION ( 'NONE',  ( 2.336881798971000105E-14, 0.000000000000000000, 1.000000000000000000 ) ) ;
#19280=EDGE_LOOP ( 'NONE', ( #18812, #9393, #6110, #2558 ) ) ;
#19314=CARTESIAN_POINT ( 'NONE',  ( 10.36831320283000046, -3640.848700000000008, 2292.781800000000203 ) ) ;
#19327=CARTESIAN_POINT ( 'NONE',  ( 12.69999999996000106, -3642.194899999999961, 2292.781800000000203 ) ) ;
#19341=FACE_OUTER_BOUND ( 'NONE', #16760, .T. ) ;
#19371=CARTESIAN_POINT ( 'NONE',  ( 12.69999999999999929, -3644.963499999999840, 2296.210799999999836 ) ) ;
#19377=AXIS2_PLACEMENT_3D ( 'NONE', #16256, #14275, #3365 ) ;
#19399=ORIENTED_EDGE ( 'NONE', *, *, #6803, .F. ) ;
#19452=DIRECTION ( 'NONE',  ( 0.000000000000000000, 1.000000000000000000, 0.000000000000000000 ) ) ;
#19529=CARTESIAN_POINT ( 'NONE',  ( 12.69999999997359197, -3636.810099999838712, 2296.433984632733427 ) ) ;
#19571=AXIS2_PLACEMENT_3D ( 'NONE', #9283, #9043, #265 ) ;
#19635=DIRECTION ( 'NONE',  ( -1.224646799141892071E-16, -1.000000000000000000, 2.336881798971000421E-14 ) ) ;
#19646=AXIS2_PLACEMENT_3D ( 'NONE', #21323, #23060, #10768 ) ;
#19656=FACE_OUTER_BOUND ( 'NONE', #4112, .T. ) ;
#19662=AXIS2_PLACEMENT_3D ( 'NONE', #17552, #1499, #23058 ) ;
#19668=VERTEX_POINT ( 'NONE', #4333 ) ;
#19698=CARTESIAN_POINT ( 'NONE',  ( 12.69999999999999929, -3639.502500000000055, 2290.241799999999785 ) ) ;
#19753=ORIENTED_EDGE ( 'NONE', *, *, #5687, .T. ) ;
#19760=EDGE_CURVE ( 'NONE', #19668, #22154, #21902, .T. ) ;
#19811=ADVANCED_FACE ( 'NONE', ( #20496 ), #1315, .T. ) ;
#19831=CARTESIAN_POINT ( 'NONE',  ( 12.69999999997567208, -3642.194900000083180, 2296.210799999999836 ) ) ;
#19840=SHAPE_REPRESENTATION ( 'Screw 6', ( #5611 ), #12740 ) ;
#19841=EDGE_CURVE ( 'NONE', #2161, #16552, #20775, .T. ) ;
#19872=EDGE_CURVE ( 'NONE', #11827, #7259, #10531, .T. ) ;
#19873=DIRECTION ( 'NONE',  ( 0.000000000000000000, 0.000000000000000000, -1.000000000000000000 ) ) ;
#19888=ADVANCED_FACE ( 'NONE', ( #3610 ), #14054, .T. ) ;
#19907=DIRECTION ( 'NONE',  ( 1.000000000000000000, 0.000000000000000000, 0.000000000000000000 ) ) ;
#19970=LINE ( 'NONE', #14467, #1924 ) ;
#20015=ADVANCED_FACE ( 'NONE', ( #18365 ), #21777, .F. ) ;
#20023=AXIS2_PLACEMENT_3D ( 'NONE', #23024, #12138, #17521 ) ;
#20060=ORIENTED_EDGE ( 'NONE', *, *, #21618, .F. ) ;
#20086=LINE ( 'NONE', #390, #2069 ) ;
#20281=CYLINDRICAL_SURFACE ( 'NONE', #6512, 3.175000000000149925 ) ;
#20287=( NAMED_UNIT ( * ) SI_UNIT ( $, .STERADIAN. ) SOLID_ANGLE_UNIT ( ) );
#20334=ORIENTED_EDGE ( 'NONE', *, *, #6126, .F. ) ;
#20351=CARTESIAN_POINT ( 'NONE',  ( 15.03168679714000078, -3638.156300000000101, 2292.781800000000203 ) ) ;
#20372=AXIS2_PLACEMENT_3D ( 'NONE', #10844, #19635, #19873 ) ;
#20382=ORIENTED_EDGE ( 'NONE', *, *, #19841, .F. ) ;
#20416=CARTESIAN_POINT ( 'NONE',  ( 15.41268679713999923, -3639.502500000000055, 2296.210799999999836 ) ) ;
#20455=ADVANCED_FACE ( 'NONE', ( #9549 ), #4393, .T. ) ;
#20494=ORIENTED_EDGE ( 'NONE', *, *, #10143, .F. ) ;
#20496=FACE_OUTER_BOUND ( 'NONE', #17621, .T. ) ;
#20522=DIRECTION ( 'NONE',  ( -1.206520773835000154E-12, -1.000000000000000000, 2.336881798973999985E-14 ) ) ;
#20534=LINE ( 'NONE', #5723, #1028 ) ;
#20677=AXIS2_PLACEMENT_3D ( 'NONE', #657, #7808, #14849 ) ;
#20723=CARTESIAN_POINT ( 'NONE',  ( 12.69999999999999929, -3639.502500000000055, 2264.841800000000148 ) ) ;
#20743=CIRCLE ( 'NONE', #20372, 0.3809999999999647002 ) ;
#20752=DIRECTION ( 'NONE',  ( 2.185478394942999951E-13, 1.295098308114000000E-13, 1.000000000000000000 ) ) ;
#20767=DIRECTION ( 'NONE',  ( 0.000000000000000000, 0.000000000000000000, -1.000000000000000000 ) ) ;
#20775=CIRCLE ( 'NONE', #18915, 5.080000000000000071 ) ;
#20794=CARTESIAN_POINT ( 'NONE',  ( 15.03168679714165634, -3638.156299999853218, 2296.433984632644751 ) ) ;
#20807=EDGE_CURVE ( 'NONE', #204, #22999, #20086, .T. ) ;
#20846=DIRECTION ( 'NONE',  ( -0.5000000000048030468, 0.8660254037816655925, 0.000000000000000000 ) ) ;
#20976=ADVANCED_FACE ( 'NONE', ( #6252 ), #13261, .T. ) ;
#21060=DIRECTION ( 'NONE',  ( 0.000000000000000000, 1.000000000000000000, 0.000000000000000000 ) ) ;
#21109=ORIENTED_EDGE ( 'NONE', *, *, #11994, .T. ) ;
#21126=( LENGTH_UNIT ( ) NAMED_UNIT ( * ) SI_UNIT ( .MILLI., .METRE. ) );
#21198=LINE ( 'NONE', #15570, #10699 ) ;
#21202=VECTOR ( 'NONE', #22143, 1000.000000000000000 ) ;
#21205=ORIENTED_EDGE ( 'NONE', *, *, #21400, .T. ) ;
#21216=ORIENTED_EDGE ( 'NONE', *, *, #9360, .F. ) ;
#21239=ORIENTED_EDGE ( 'NONE', *, *, #81, .F. ) ;
#21272=ADVANCED_FACE ( 'NONE', ( #11335 ), #5965, .T. ) ;
#21284=MANIFOLD_SOLID_BREP ( 'SOLID21[1]', #867 ) ;
#21323=CARTESIAN_POINT ( 'NONE',  ( 12.69999999999999929, -3639.502500000000055, 2290.622800000000097 ) ) ;
#21330=CARTESIAN_POINT ( 'NONE',  ( 12.69999999999999929, -3639.502500000000055, 2264.841800000000148 ) ) ;
#21332=DIRECTION ( 'NONE',  ( -1.000000000000000000, 2.331176954593508450E-12, 0.000000000000000000 ) ) ;
#21339=FACE_OUTER_BOUND ( 'NONE', #2621, .T. ) ;
#21400=EDGE_CURVE ( 'NONE', #2236, #671, #4768, .T. ) ;
#21424=CARTESIAN_POINT ( 'NONE',  ( 12.69999999999999929, -3639.502500000000055, 2290.622800000000097 ) ) ;
#21429=ORIENTED_EDGE ( 'NONE', *, *, #7092, .F. ) ;
#21462=CIRCLE ( 'NONE', #16225, 3.175000000000149925 ) ;
#21505=CARTESIAN_POINT ( 'NONE',  ( 12.69999999999999929, -3639.502500000000055, 2296.210799999999836 ) ) ;
#21526=CARTESIAN_POINT ( 'NONE',  ( 12.69999999999999929, -3639.502500000000055, 2264.841800000000148 ) ) ;
#21532=ORIENTED_EDGE ( 'NONE', *, *, #19760, .F. ) ;
#21564=CYLINDRICAL_SURFACE ( 'NONE', #10374, 0.3809999999999993947 ) ;
#21599=EDGE_LOOP ( 'NONE', ( #21216, #14368, #3575, #1113 ) ) ;
#21618=EDGE_CURVE ( 'NONE', #7858, #204, #15937, .T. ) ;
#21652=CARTESIAN_POINT ( 'NONE',  ( 15.03168679714000078, -3638.156300000000101, 2296.210799999999836 ) ) ;
#21680=CYLINDRICAL_SURFACE ( 'NONE', #22187, 5.460999999999938126 ) ;
#21703=EDGE_LOOP ( 'NONE', ( #14774, #9680, #22135, #21715 ) ) ;
#21715=ORIENTED_EDGE ( 'NONE', *, *, #22968, .F. ) ;
#21726=EDGE_CURVE ( 'NONE', #3332, #22386, #9446, .T. ) ;
#21734=ORIENTED_EDGE ( 'NONE', *, *, #22968, .T. ) ;
#21772=EDGE_CURVE ( 'NONE', #2000, #2498, #12589, .T. ) ;
#21773=ORIENTED_EDGE ( 'NONE', *, *, #1350, .T. ) ;
#21777=PLANE ( 'NONE',  #2839 ) ;
#21780=VECTOR ( 'NONE', #17487, 1000.000000000000114 ) ;
#21807=DIRECTION ( 'NONE',  ( 0.000000000000000000, 1.000000000000000000, 0.000000000000000000 ) ) ;
#21851=EDGE_CURVE ( 'NONE', #18372, #4050, #2741, .T. ) ;
#21886=DIRECTION ( 'NONE',  ( 0.000000000000000000, 0.000000000000000000, 1.000000000000000000 ) ) ;
#21902=CIRCLE ( 'NONE', #217, 5.080000000000000959 ) ;
#21967=CARTESIAN_POINT ( 'NONE',  ( 12.69999999994000106, -3636.810100000000148, 2292.781800000000203 ) ) ;
#22078=ORIENTED_EDGE ( 'NONE', *, *, #19872, .F. ) ;
#22083=CARTESIAN_POINT ( 'NONE',  ( 10.36831320283000046, -3640.848700000000008, 2292.781800000000203 ) ) ;
#22099=ORIENTED_EDGE ( 'NONE', *, *, #9764, .T. ) ;
#22113=FACE_OUTER_BOUND ( 'NONE', #6016, .T. ) ;
#22135=ORIENTED_EDGE ( 'NONE', *, *, #21851, .T. ) ;
#22143=DIRECTION ( 'NONE',  ( 0.000000000000000000, 0.000000000000000000, 1.000000000000000000 ) ) ;
#22154=VERTEX_POINT ( 'NONE', #8958 ) ;
#22187=AXIS2_PLACEMENT_3D ( 'NONE', #19698, #5636, #12771 ) ;
#22236=AXIS2_PLACEMENT_3D ( 'NONE', #1331, #6508, #6859 ) ;
#22265=ORIENTED_EDGE ( 'NONE', *, *, #17557, .F. ) ;
#22271=VECTOR ( 'NONE', #20752, 1000.000000000000000 ) ;
#22310=DIRECTION ( 'NONE',  ( 1.148603104910000072E-12, 1.000000000000000000, 0.000000000000000000 ) ) ;
#22351=DIRECTION ( 'NONE',  ( 0.000000000000000000, 0.000000000000000000, 1.000000000000000000 ) ) ;
#22381=ADVANCED_FACE ( 'NONE', ( #4427, #22113 ), #11453, .F. ) ;
#22386=VERTEX_POINT ( 'NONE', #7596 ) ;
#22476=DIRECTION ( 'NONE',  ( 0.8660254037815640071, 0.5000000000049790172, 0.000000000000000000 ) ) ;
#22490=( BOUNDED_CURVE ( )  B_SPLINE_CURVE ( 3, ( #19831, #7073, #12451, #5309 ),
 .UNSPECIFIED., .F., .F. ) 
 B_SPLINE_CURVE_WITH_KNOTS ( ( 4, 4 ),
 ( 3.686081134657729747E-14, 1.570796326492095440 ),
 .UNSPECIFIED. ) 
 CURVE ( )  GEOMETRIC_REPRESENTATION_ITEM ( )  RATIONAL_B_SPLINE_CURVE ( ( 1.000000000000000000, 0.8047378541957446174, 0.8047378541957446174, 1.000000000000000000 ) ) 
 REPRESENTATION_ITEM ( '' )  );
#22501=CARTESIAN_POINT ( 'NONE',  ( 12.69999999997359019, -3636.810099999929662, 2296.210799999999836 ) ) ;
#22552=CARTESIAN_POINT ( 'NONE',  ( 10.21049783553828050, -3638.065185255057713, 2296.591800000037438 ) ) ;
#22635=LINE ( 'NONE', #6376, #21780 ) ;
#22665=ORIENTED_EDGE ( 'NONE', *, *, #2664, .T. ) ;
#22669=CARTESIAN_POINT ( 'NONE',  ( 10.36831320283682167, -3638.156299999849125, 2296.433984632765714 ) ) ;
#22794=DIRECTION ( 'NONE',  ( 2.336881798971000105E-14, 0.000000000000000000, 1.000000000000000000 ) ) ;
#22803=VERTEX_POINT ( 'NONE', #22083 ) ;
#22834=EDGE_LOOP ( 'NONE', ( #252, #5508, #15169, #170 ) ) ;
#22850=CARTESIAN_POINT ( 'NONE',  ( 12.69999999999999929, -3639.502500000000055, 2264.841800000000148 ) ) ;
#22873=EDGE_LOOP ( 'NONE', ( #18978, #15012, #5089, #8718, #14978, #16805 ) ) ;
#22877=VECTOR ( 'NONE', #11401, 1000.000000000000000 ) ;
#22894=SHAPE_DEFINITION_REPRESENTATION ( #1512, #19840 ) ;
#22968=EDGE_CURVE ( 'NONE', #22999, #4050, #7861, .T. ) ;
#22980=AXIS2_PLACEMENT_3D ( 'NONE', #15670, #22794, #6659 ) ;
#22999=VERTEX_POINT ( 'NONE', #19042 ) ;
#23024=CARTESIAN_POINT ( 'NONE',  ( 12.69999999999999929, -3639.502500000000055, 2296.210799999999836 ) ) ;
#23058=DIRECTION ( 'NONE',  ( 0.000000000000000000, -1.000000000000000000, 0.000000000000000000 ) ) ;
#23060=DIRECTION ( 'NONE',  ( -2.336881798971000105E-14, 0.000000000000000000, -1.000000000000000000 ) ) ;
#23064=ORIENTED_EDGE ( 'NONE', *, *, #7004, .T. ) ;
#23077=AXIS2_PLACEMENT_3D ( 'NONE', #21505, #5454, #17978 ) ;
#23089=ORIENTED_EDGE ( 'NONE', *, *, #9430, .F. ) ;
#23091=AXIS2_PLACEMENT_3D ( 'NONE', #3886, #12792, #16197 ) ;
#23094=( NAMED_UNIT ( * ) SI_UNIT ( $, .STERADIAN. ) SOLID_ANGLE_UNIT ( ) );
#23208=COLOUR_RGB('Black',0.12,0.14,0.17);
#23209=FILL_AREA_STYLE_COLOUR('',#23208);
#23210=FILL_AREA_STYLE('',(#23209));
#23211=SURFACE_STYLE_FILL_AREA(#23210);
#23212=SURFACE_SIDE_STYLE('',(#23211));
#23213=SURFACE_STYLE_USAGE(.BOTH.,#23212);
#23214=PRESENTATION_STYLE_ASSIGNMENT((#23213));
#23230=STYLED_ITEM('',(#23214),#21284);
#23237=MECHANICAL_DESIGN_GEOMETRIC_PRESENTATION_REPRESENTATION('',(#23230),#2257);
ENDSEC;
END-ISO-10303-21;
